ISO-10303-21;
HEADER;
/* Generated by software containing ST-Developer
 * from STEP Tools, Inc. (www.steptools.com) 
 */

FILE_DESCRIPTION(
/* description */ ('Fatigue rig crank-slider'),
/* implementation_level */ '2;1');

FILE_NAME(
/* name */ 'Flat Washer - M5.step',
/* time_stamp */ '2026-10-28T03:24:50-07:00',
/* author */ (''),
/* organization */ (''),
/* preprocessor_version */ 'ST-DEVELOPER v20.2',
/* originating_system */ 'Autodesk Translation Framework v15.17.0.0',
/* authorisation */ '');

FILE_SCHEMA (('AUTOMOTIVE_DESIGN { 1 0 10303 214 3 1 1 }'));
ENDSEC;

DATA;
#10=MECHANICAL_DESIGN_GEOMETRIC_PRESENTATION_REPRESENTATION('',(#643),#16911);
#29=CONICAL_SURFACE('',#10431,0.275,0.785398163397449);
#534=SHAPE_REPRESENTATION_RELATIONSHIP('SRR','None',#17179,#584);
#584=ADVANCED_BREP_SHAPE_REPRESENTATION('',(#699),#16908);
#643=STYLED_ITEM('',(#17494),#699);
#699=MANIFOLD_SOLID_BREP('Body1',#8937);
#893=FACE_BOUND('',#2421,.T.);
#894=FACE_BOUND('',#2424,.T.);
#1193=PLANE('',#10436);
#1194=PLANE('',#10440);
#1702=FACE_OUTER_BOUND('',#2418,.T.);
#1703=FACE_OUTER_BOUND('',#2419,.T.);
#1704=FACE_OUTER_BOUND('',#2420,.T.);
#1705=FACE_OUTER_BOUND('',#2422,.T.);
#1706=FACE_OUTER_BOUND('',#2423,.T.);
#2418=EDGE_LOOP('',(#8056,#8057,#8058,#8059));
#2419=EDGE_LOOP('',(#8060,#8061,#8062,#8063));
#2420=EDGE_LOOP('',(#8064));
#2421=EDGE_LOOP('',(#8065));
#2422=EDGE_LOOP('',(#8066,#8067,#8068,#8069));
#2423=EDGE_LOOP('',(#8070));
#2424=EDGE_LOOP('',(#8071));
#3056=LINE('',#16569,#3702);
#3057=LINE('',#16573,#3703);
#3058=LINE('',#16580,#3704);
#3702=VECTOR('',#13042,0.275);
#3703=VECTOR('',#13047,0.265);
#3704=VECTOR('',#13056,0.5);
#4132=CIRCLE('',#10432,0.285);
#4133=CIRCLE('',#10433,0.265);
#4134=CIRCLE('',#10435,0.265);
#4135=CIRCLE('',#10437,0.5);
#4136=CIRCLE('',#10439,0.5);
#4852=VERTEX_POINT('',#16566);
#4853=VERTEX_POINT('',#16568);
#4854=VERTEX_POINT('',#16572);
#4855=VERTEX_POINT('',#16576);
#4856=VERTEX_POINT('',#16579);
#5926=EDGE_CURVE('',#4852,#4852,#4132,.T.);
#5927=EDGE_CURVE('',#4852,#4853,#3056,.T.);
#5928=EDGE_CURVE('',#4853,#4853,#4133,.T.);
#5929=EDGE_CURVE('',#4853,#4854,#3057,.T.);
#5930=EDGE_CURVE('',#4854,#4854,#4134,.T.);
#5931=EDGE_CURVE('',#4855,#4855,#4135,.T.);
#5932=EDGE_CURVE('',#4855,#4856,#3058,.T.);
#5933=EDGE_CURVE('',#4856,#4856,#4136,.T.);
#8056=ORIENTED_EDGE('',*,*,#5926,.T.);
#8057=ORIENTED_EDGE('',*,*,#5927,.T.);
#8058=ORIENTED_EDGE('',*,*,#5928,.T.);
#8059=ORIENTED_EDGE('',*,*,#5927,.F.);
#8060=ORIENTED_EDGE('',*,*,#5928,.F.);
#8061=ORIENTED_EDGE('',*,*,#5929,.T.);
#8062=ORIENTED_EDGE('',*,*,#5930,.T.);
#8063=ORIENTED_EDGE('',*,*,#5929,.F.);
#8064=ORIENTED_EDGE('',*,*,#5931,.T.);
#8065=ORIENTED_EDGE('',*,*,#5926,.F.);
#8066=ORIENTED_EDGE('',*,*,#5931,.F.);
#8067=ORIENTED_EDGE('',*,*,#5932,.T.);
#8068=ORIENTED_EDGE('',*,*,#5933,.T.);
#8069=ORIENTED_EDGE('',*,*,#5932,.F.);
#8070=ORIENTED_EDGE('',*,*,#5933,.F.);
#8071=ORIENTED_EDGE('',*,*,#5930,.F.);
#8349=CYLINDRICAL_SURFACE('',#10434,0.265);
#8350=CYLINDRICAL_SURFACE('',#10438,0.5);
#8840=ADVANCED_FACE('',(#1702),#29,.F.);
#8841=ADVANCED_FACE('',(#1703),#8349,.F.);
#8842=ADVANCED_FACE('',(#1704,#893),#1193,.T.);
#8843=ADVANCED_FACE('',(#1705),#8350,.T.);
#8844=ADVANCED_FACE('',(#1706,#894),#1194,.F.);
#8937=CLOSED_SHELL('',(#8840,#8841,#8842,#8843,#8844));
#10430=AXIS2_PLACEMENT_3D('',#16564,#13036,#13037);
#10431=AXIS2_PLACEMENT_3D('',#16565,#13038,#13039);
#10432=AXIS2_PLACEMENT_3D('',#16567,#13040,#13041);
#10433=AXIS2_PLACEMENT_3D('',#16570,#13043,#13044);
#10434=AXIS2_PLACEMENT_3D('',#16571,#13045,#13046);
#10435=AXIS2_PLACEMENT_3D('',#16574,#13048,#13049);
#10436=AXIS2_PLACEMENT_3D('',#16575,#13050,#13051);
#10437=AXIS2_PLACEMENT_3D('',#16577,#13052,#13053);
#10438=AXIS2_PLACEMENT_3D('',#16578,#13054,#13055);
#10439=AXIS2_PLACEMENT_3D('',#16581,#13057,#13058);
#10440=AXIS2_PLACEMENT_3D('',#16582,#13059,#13060);
#13036=DIRECTION('axis',(0.,0.,1.));
#13037=DIRECTION('refdir',(1.,0.,0.));
#13038=DIRECTION('center_axis',(0.,1.,0.));
#13039=DIRECTION('ref_axis',(1.,0.,0.));
#13040=DIRECTION('center_axis',(0.,1.,0.));
#13041=DIRECTION('ref_axis',(1.,0.,0.));
#13042=DIRECTION('',(0.707106781186548,-0.707106781186547,-8.65956056235494E-17));
#13043=DIRECTION('center_axis',(0.,-1.,0.));
#13044=DIRECTION('ref_axis',(1.,0.,0.));
#13045=DIRECTION('center_axis',(0.,1.,0.));
#13046=DIRECTION('ref_axis',(1.,0.,0.));
#13047=DIRECTION('',(0.,-1.,0.));
#13048=DIRECTION('center_axis',(0.,-1.,0.));
#13049=DIRECTION('ref_axis',(1.,0.,0.));
#13050=DIRECTION('center_axis',(0.,1.,0.));
#13051=DIRECTION('ref_axis',(1.,0.,0.));
#13052=DIRECTION('center_axis',(0.,1.,0.));
#13053=DIRECTION('ref_axis',(1.,0.,0.));
#13054=DIRECTION('center_axis',(0.,1.,0.));
#13055=DIRECTION('ref_axis',(1.,0.,0.));
#13056=DIRECTION('',(0.,-1.,0.));
#13057=DIRECTION('center_axis',(0.,1.,0.));
#13058=DIRECTION('ref_axis',(1.,0.,0.));
#13059=DIRECTION('center_axis',(0.,1.,0.));
#13060=DIRECTION('ref_axis',(1.,0.,0.));
#16564=CARTESIAN_POINT('',(0.,0.,0.));
#16565=CARTESIAN_POINT('Origin',(0.,0.09,0.));
#16566=CARTESIAN_POINT('',(-0.285,0.1,3.49024337756996E-17));
#16567=CARTESIAN_POINT('Origin',(0.,0.1,0.));
#16568=CARTESIAN_POINT('',(-0.265,0.08,-3.24531401774049E-17));
#16569=CARTESIAN_POINT('',(-0.275,0.09,3.36777869765522E-17));
#16570=CARTESIAN_POINT('Origin',(0.,0.08,0.));
#16571=CARTESIAN_POINT('Origin',(0.,0.,0.));
#16572=CARTESIAN_POINT('',(-0.265,0.,3.24531401774049E-17));
#16573=CARTESIAN_POINT('',(-0.265,0.,3.24531401774049E-17));
#16574=CARTESIAN_POINT('Origin',(0.,0.,0.));
#16575=CARTESIAN_POINT('Origin',(0.,0.1,0.));
#16576=CARTESIAN_POINT('',(-0.5,0.1,6.12323399573677E-17));
#16577=CARTESIAN_POINT('Origin',(0.,0.1,0.));
#16578=CARTESIAN_POINT('Origin',(0.,0.,0.));
#16579=CARTESIAN_POINT('',(-0.5,0.,6.12323399573677E-17));
#16580=CARTESIAN_POINT('',(-0.5,0.,6.12323399573677E-17));
#16581=CARTESIAN_POINT('Origin',(0.,0.,0.));
#16582=CARTESIAN_POINT('Origin',(0.,0.,0.));
#16849=UNCERTAINTY_MEASURE_WITH_UNIT(LENGTH_MEASURE(0.001),#16912,
'DISTANCE_ACCURACY_VALUE',
'Maximum model space distance between geometric entities at asserted c
onnectivities');
#16852=UNCERTAINTY_MEASURE_WITH_UNIT(LENGTH_MEASURE(0.001),#16912,
'DISTANCE_ACCURACY_VALUE',
'Maximum model space distance between geometric entities at asserted c
onnectivities');
#16908=(
GEOMETRIC_REPRESENTATION_CONTEXT(3)
GLOBAL_UNCERTAINTY_ASSIGNED_CONTEXT((#16849))
GLOBAL_UNIT_ASSIGNED_CONTEXT((#16912,#16914,#16915))
REPRESENTATION_CONTEXT('','3D')
);
#16911=(
GEOMETRIC_REPRESENTATION_CONTEXT(3)
GLOBAL_UNCERTAINTY_ASSIGNED_CONTEXT((#16852))
GLOBAL_UNIT_ASSIGNED_CONTEXT((#16912,#16914,#16915))
REPRESENTATION_CONTEXT('','3D')
);
#16912=(
LENGTH_UNIT()
NAMED_UNIT(*)
SI_UNIT(.CENTI.,.METRE.)
);
#16914=(
NAMED_UNIT(*)
PLANE_ANGLE_UNIT()
SI_UNIT($,.RADIAN.)
);
#16915=(
NAMED_UNIT(*)
SI_UNIT($,.STERADIAN.)
SOLID_ANGLE_UNIT()
);
#16971=SHAPE_DEFINITION_REPRESENTATION(#17046,#17179);
#17046=PRODUCT_DEFINITION_SHAPE('',$,#17238);
#17179=SHAPE_REPRESENTATION('',(#10430),#16908);
#17182=PRODUCT_DEFINITION_CONTEXT('part definition',#17358,'design');
#17238=PRODUCT_DEFINITION('Flat Washer - M5','Flat Washer - M5',#17296,
#17182);
#17296=PRODUCT_DEFINITION_FORMATION('',$,#17415);
#17358=APPLICATION_CONTEXT(
'Core Data for Automotive Mechanical Design Process');
#17359=PRODUCT_CONTEXT('part definition',#17358,'mechanical');
#17415=PRODUCT('Flat Washer - M5','Flat Washer - M5','Flat Washer - M5',
(#17359));
#17488=COLOUR_RGB('Black',0.12,0.14,0.17);
#17489=FILL_AREA_STYLE_COLOUR('',#17488);
#17490=FILL_AREA_STYLE('',(#17489));
#17491=SURFACE_STYLE_FILL_AREA(#17490);
#17492=SURFACE_SIDE_STYLE('',(#17491));
#17493=SURFACE_STYLE_USAGE(.BOTH.,#17492);
#17494=PRESENTATION_STYLE_ASSIGNMENT((#17493));
ENDSEC;
END-ISO-10303-21;
